ISO-10303-21;
HEADER;
FILE_DESCRIPTION((''),'2;1');
FILE_NAME('BRACKET_BOLT_M8x16.step','2026-10-01T22:05:39-07:00',(''),(''),'','','');
FILE_SCHEMA (('AUTOMOTIVE_DESIGN { 1 0 10303 214 3 1 1 }'));
ENDSEC;
DATA;
#10=MECHANICAL_DESIGN_GEOMETRIC_PRESENTATION_REPRESENTATION('',(#644),#24628);
#560=SHAPE_REPRESENTATION_RELATIONSHIP('SRR','None',#24835,#602) ;
#602=ADVANCED_BREP_SHAPE_REPRESENTATION('',(#683),#24625) ;
#644=STYLED_ITEM('',(#25030),#683) ;
#683=MANIFOLD_SOLID_BREP('BRACKET_BOLT_M8x16',#13186) ;
#947=FACE_BOUND('',#4728,.T.) ;
#1780=LINE('',#24378,#2616) ;
#1781=LINE('',#24384,#2617) ;
#1782=LINE('',#24386,#2618) ;
#1783=LINE('',#24388,#2619) ;
#1784=LINE('',#24389,#2620) ;
#1785=LINE('',#24393,#2621) ;
#1786=LINE('',#24395,#2622) ;
#1787=LINE('',#24397,#2623) ;
#1788=LINE('',#24398,#2624) ;
#1789=LINE('',#24401,#2625) ;
#1790=LINE('',#24402,#2626) ;
#1791=LINE('',#24404,#2627) ;
#1792=LINE('',#24405,#2628) ;
#1793=LINE('',#24408,#2629) ;
#1794=LINE('',#24409,#2630) ;
#1795=LINE('',#24412,#2631) ;
#1796=LINE('',#24413,#2632) ;
#1797=LINE('',#24415,#2633) ;
#1798=LINE('',#24417,#2634) ;
#2616=VECTOR('',#19529,0.4) ;
#2617=VECTOR('',#19536,1.) ;
#2618=VECTOR('',#19537,1.) ;
#2619=VECTOR('',#19538,1.) ;
#2620=VECTOR('',#19539,1.) ;
#2621=VECTOR('',#19542,1.) ;
#2622=VECTOR('',#19543,1.) ;
#2623=VECTOR('',#19544,1.) ;
#2624=VECTOR('',#19545,1.) ;
#2625=VECTOR('',#19548,1.) ;
#2626=VECTOR('',#19549,1.) ;
#2627=VECTOR('',#19550,1.) ;
#2628=VECTOR('',#19551,1.) ;
#2629=VECTOR('',#19554,1.) ;
#2630=VECTOR('',#19555,1.) ;
#2631=VECTOR('',#19558,1.) ;
#2632=VECTOR('',#19559,1.) ;
#2633=VECTOR('',#19562,1.) ;
#2634=VECTOR('',#19565,1.) ;
#2949=CYLINDRICAL_SURFACE('',#15330,0.4) ;
#3690=FACE_OUTER_BOUND('',#4718,.T.) ;
#3691=FACE_OUTER_BOUND('',#4719,.T.) ;
#3692=FACE_OUTER_BOUND('',#4720,.T.) ;
#3693=FACE_OUTER_BOUND('',#4721,.T.) ;
#3694=FACE_OUTER_BOUND('',#4722,.T.) ;
#3695=FACE_OUTER_BOUND('',#4723,.T.) ;
#3696=FACE_OUTER_BOUND('',#4724,.T.) ;
#3697=FACE_OUTER_BOUND('',#4725,.T.) ;
#3698=FACE_OUTER_BOUND('',#4726,.T.) ;
#3699=FACE_OUTER_BOUND('',#4727,.T.) ;
#4718=EDGE_LOOP('',(#11869,#11870,#11871,#11872)) ;
#4719=EDGE_LOOP('',(#11873)) ;
#4720=EDGE_LOOP('',(#11874,#11875,#11876,#11877)) ;
#4721=EDGE_LOOP('',(#11878,#11879,#11880,#11881)) ;
#4722=EDGE_LOOP('',(#11882,#11883,#11884,#11885,#11886,#11887)) ;
#4723=EDGE_LOOP('',(#11888,#11889,#11890,#11891)) ;
#4724=EDGE_LOOP('',(#11892,#11893,#11894,#11895)) ;
#4725=EDGE_LOOP('',(#11896,#11897,#11898,#11899)) ;
#4726=EDGE_LOOP('',(#11900,#11901,#11902,#11903)) ;
#4727=EDGE_LOOP('',(#11904,#11905,#11906,#11907,#11908,#11909)) ;
#4728=EDGE_LOOP('',(#11910)) ;
#5531=CIRCLE('',#15331,0.4) ;
#5532=CIRCLE('',#15332,0.4) ;
#6691=VERTEX_POINT('',#24375) ;
#6692=VERTEX_POINT('',#24377) ;
#6693=VERTEX_POINT('',#24382) ;
#6694=VERTEX_POINT('',#24383) ;
#6695=VERTEX_POINT('',#24385) ;
#6696=VERTEX_POINT('',#24387) ;
#6697=VERTEX_POINT('',#24391) ;
#6698=VERTEX_POINT('',#24392) ;
#6699=VERTEX_POINT('',#24394) ;
#6700=VERTEX_POINT('',#24396) ;
#6701=VERTEX_POINT('',#24400) ;
#6702=VERTEX_POINT('',#24403) ;
#6703=VERTEX_POINT('',#24407) ;
#6704=VERTEX_POINT('',#24411) ;
#8424=EDGE_CURVE('',#6691,#6691,#5531,.T.) ;
#8425=EDGE_CURVE('',#6691,#6692,#1780,.T.) ;
#8426=EDGE_CURVE('',#6692,#6692,#5532,.T.) ;
#8427=EDGE_CURVE('',#6693,#6694,#1781,.T.) ;
#8428=EDGE_CURVE('',#6693,#6695,#1782,.T.) ;
#8429=EDGE_CURVE('',#6696,#6695,#1783,.T.) ;
#8430=EDGE_CURVE('',#6696,#6694,#1784,.T.) ;
#8431=EDGE_CURVE('',#6697,#6698,#1785,.T.) ;
#8432=EDGE_CURVE('',#6697,#6699,#1786,.T.) ;
#8433=EDGE_CURVE('',#6700,#6699,#1787,.T.) ;
#8434=EDGE_CURVE('',#6700,#6698,#1788,.T.) ;
#8435=EDGE_CURVE('',#6701,#6693,#1789,.T.) ;
#8436=EDGE_CURVE('',#6699,#6701,#1790,.T.) ;
#8437=EDGE_CURVE('',#6702,#6697,#1791,.T.) ;
#8438=EDGE_CURVE('',#6695,#6702,#1792,.T.) ;
#8439=EDGE_CURVE('',#6701,#6703,#1793,.T.) ;
#8440=EDGE_CURVE('',#6694,#6703,#1794,.T.) ;
#8441=EDGE_CURVE('',#6702,#6704,#1795,.T.) ;
#8442=EDGE_CURVE('',#6698,#6704,#1796,.T.) ;
#8443=EDGE_CURVE('',#6703,#6700,#1797,.T.) ;
#8444=EDGE_CURVE('',#6704,#6696,#1798,.T.) ;
#11869=ORIENTED_EDGE('',*,*,#8424,.F.) ;
#11870=ORIENTED_EDGE('',*,*,#8425,.T.) ;
#11871=ORIENTED_EDGE('',*,*,#8426,.F.) ;
#11872=ORIENTED_EDGE('',*,*,#8425,.F.) ;
#11873=ORIENTED_EDGE('',*,*,#8424,.T.) ;
#11874=ORIENTED_EDGE('',*,*,#8427,.F.) ;
#11875=ORIENTED_EDGE('',*,*,#8428,.T.) ;
#11876=ORIENTED_EDGE('',*,*,#8429,.F.) ;
#11877=ORIENTED_EDGE('',*,*,#8430,.T.) ;
#11878=ORIENTED_EDGE('',*,*,#8431,.F.) ;
#11879=ORIENTED_EDGE('',*,*,#8432,.T.) ;
#11880=ORIENTED_EDGE('',*,*,#8433,.F.) ;
#11881=ORIENTED_EDGE('',*,*,#8434,.T.) ;
#11882=ORIENTED_EDGE('',*,*,#8428,.F.) ;
#11883=ORIENTED_EDGE('',*,*,#8435,.F.) ;
#11884=ORIENTED_EDGE('',*,*,#8436,.F.) ;
#11885=ORIENTED_EDGE('',*,*,#8432,.F.) ;
#11886=ORIENTED_EDGE('',*,*,#8437,.F.) ;
#11887=ORIENTED_EDGE('',*,*,#8438,.F.) ;
#11888=ORIENTED_EDGE('',*,*,#8439,.F.) ;
#11889=ORIENTED_EDGE('',*,*,#8435,.T.) ;
#11890=ORIENTED_EDGE('',*,*,#8427,.T.) ;
#11891=ORIENTED_EDGE('',*,*,#8440,.T.) ;
#11892=ORIENTED_EDGE('',*,*,#8441,.F.) ;
#11893=ORIENTED_EDGE('',*,*,#8437,.T.) ;
#11894=ORIENTED_EDGE('',*,*,#8431,.T.) ;
#11895=ORIENTED_EDGE('',*,*,#8442,.T.) ;
#11896=ORIENTED_EDGE('',*,*,#8439,.T.) ;
#11897=ORIENTED_EDGE('',*,*,#8443,.T.) ;
#11898=ORIENTED_EDGE('',*,*,#8433,.T.) ;
#11899=ORIENTED_EDGE('',*,*,#8436,.T.) ;
#11900=ORIENTED_EDGE('',*,*,#8429,.T.) ;
#11901=ORIENTED_EDGE('',*,*,#8438,.T.) ;
#11902=ORIENTED_EDGE('',*,*,#8441,.T.) ;
#11903=ORIENTED_EDGE('',*,*,#8444,.T.) ;
#11904=ORIENTED_EDGE('',*,*,#8430,.F.) ;
#11905=ORIENTED_EDGE('',*,*,#8444,.F.) ;
#11906=ORIENTED_EDGE('',*,*,#8442,.F.) ;
#11907=ORIENTED_EDGE('',*,*,#8434,.F.) ;
#11908=ORIENTED_EDGE('',*,*,#8443,.F.) ;
#11909=ORIENTED_EDGE('',*,*,#8440,.F.) ;
#11910=ORIENTED_EDGE('',*,*,#8426,.T.) ;
#12321=PLANE('',#15333) ;
#12322=PLANE('',#15334) ;
#12323=PLANE('',#15335) ;
#12324=PLANE('',#15336) ;
#12325=PLANE('',#15337) ;
#12326=PLANE('',#15338) ;
#12327=PLANE('',#15339) ;
#12328=PLANE('',#15340) ;
#12329=PLANE('',#15341) ;
#13085=ADVANCED_FACE('',(#3690),#2949,.T.) ;
#13086=ADVANCED_FACE('',(#3691),#12321,.T.) ;
#13087=ADVANCED_FACE('',(#3692),#12322,.F.) ;
#13088=ADVANCED_FACE('',(#3693),#12323,.F.) ;
#13089=ADVANCED_FACE('',(#3694),#12324,.T.) ;
#13090=ADVANCED_FACE('',(#3695),#12325,.F.) ;
#13091=ADVANCED_FACE('',(#3696),#12326,.F.) ;
#13092=ADVANCED_FACE('',(#3697),#12327,.F.) ;
#13093=ADVANCED_FACE('',(#3698),#12328,.F.) ;
#13094=ADVANCED_FACE('',(#3699,#947),#12329,.T.) ;
#13186=CLOSED_SHELL('',(#13085,#13086,#13087,#13088,#13089,#13090,#13091,
#13092,#13093,#13094)) ;
#15329=AXIS2_PLACEMENT_3D('',#24373,#19523,#19524) ;
#15330=AXIS2_PLACEMENT_3D('',#24374,#19525,#19526) ;
#15331=AXIS2_PLACEMENT_3D('',#24376,#19527,#19528) ;
#15332=AXIS2_PLACEMENT_3D('',#24379,#19530,#19531) ;
#15333=AXIS2_PLACEMENT_3D('',#24380,#19532,#19533) ;
#15334=AXIS2_PLACEMENT_3D('',#24381,#19534,#19535) ;
#15335=AXIS2_PLACEMENT_3D('',#24390,#19540,#19541) ;
#15336=AXIS2_PLACEMENT_3D('',#24399,#19546,#19547) ;
#15337=AXIS2_PLACEMENT_3D('',#24406,#19552,#19553) ;
#15338=AXIS2_PLACEMENT_3D('',#24410,#19556,#19557) ;
#15339=AXIS2_PLACEMENT_3D('',#24414,#19560,#19561) ;
#15340=AXIS2_PLACEMENT_3D('',#24416,#19563,#19564) ;
#15341=AXIS2_PLACEMENT_3D('',#24418,#19566,#19567) ;
#19523=DIRECTION('axis',(0.,0.,1.)) ;
#19524=DIRECTION('refdir',(1.,0.,0.)) ;
#19525=DIRECTION('center_axis',(0.,1.,0.)) ;
#19526=DIRECTION('ref_axis',(1.,0.,0.)) ;
#19527=DIRECTION('center_axis',(0.,1.,0.)) ;
#19528=DIRECTION('ref_axis',(1.,0.,0.)) ;
#19529=DIRECTION('',(0.,-1.,0.)) ;
#19530=DIRECTION('center_axis',(0.,-1.,0.)) ;
#19531=DIRECTION('ref_axis',(1.,0.,0.)) ;
#19532=DIRECTION('center_axis',(0.,1.,0.)) ;
#19533=DIRECTION('ref_axis',(1.,0.,0.)) ;
#19534=DIRECTION('center_axis',(-0.5,0.,-0.866025403784439)) ;
#19535=DIRECTION('ref_axis',(-0.866025403784439,0.,0.5)) ;
#19536=DIRECTION('',(0.,1.,0.)) ;
#19537=DIRECTION('',(0.866025403784439,0.,-0.5)) ;
#19538=DIRECTION('',(0.,-1.,0.)) ;
#19539=DIRECTION('',(-0.866025403784439,0.,0.5)) ;
#19540=DIRECTION('center_axis',(0.5,0.,0.866025403784439)) ;
#19541=DIRECTION('ref_axis',(0.866025403784439,0.,-0.5)) ;
#19542=DIRECTION('',(0.,1.,0.)) ;
#19543=DIRECTION('',(-0.866025403784439,0.,0.5)) ;
#19544=DIRECTION('',(0.,-1.,0.)) ;
#19545=DIRECTION('',(0.866025403784439,0.,-0.5)) ;
#19546=DIRECTION('center_axis',(0.,-1.,0.)) ;
#19547=DIRECTION('ref_axis',(-1.,0.,0.)) ;
#19548=DIRECTION('',(0.866025403784439,0.,0.5)) ;
#19549=DIRECTION('',(0.,0.,1.)) ;
#19550=DIRECTION('',(-0.866025403784439,0.,-0.5)) ;
#19551=DIRECTION('',(0.,0.,-1.)) ;
#19552=DIRECTION('center_axis',(0.5,0.,-0.866025403784439)) ;
#19553=DIRECTION('ref_axis',(-0.866025403784439,0.,-0.5)) ;
#19554=DIRECTION('',(0.,1.,0.)) ;
#19555=DIRECTION('',(-0.866025403784439,0.,-0.5)) ;
#19556=DIRECTION('center_axis',(-0.5,0.,0.866025403784439)) ;
#19557=DIRECTION('ref_axis',(0.866025403784439,0.,0.5)) ;
#19558=DIRECTION('',(0.,1.,0.)) ;
#19559=DIRECTION('',(0.866025403784439,0.,0.5)) ;
#19560=DIRECTION('center_axis',(1.,0.,0.)) ;
#19561=DIRECTION('ref_axis',(0.,0.,-1.)) ;
#19562=DIRECTION('',(0.,0.,-1.)) ;
#19563=DIRECTION('center_axis',(-1.,0.,0.)) ;
#19564=DIRECTION('ref_axis',(0.,0.,1.)) ;
#19565=DIRECTION('',(0.,0.,1.)) ;
#19566=DIRECTION('center_axis',(0.,1.,0.)) ;
#19567=DIRECTION('ref_axis',(1.,0.,0.)) ;
#24373=CARTESIAN_POINT('',(0.,0.,0.)) ;
#24374=CARTESIAN_POINT('Origin',(0.,0.8,0.)) ;
#24375=CARTESIAN_POINT('',(-0.4,1.6,4.89858719658941E-17)) ;
#24376=CARTESIAN_POINT('Origin',(0.,1.6,0.)) ;
#24377=CARTESIAN_POINT('',(-0.4,0.,4.89858719658941E-17)) ;
#24378=CARTESIAN_POINT('',(-0.4,0.8,4.89858719658941E-17)) ;
#24379=CARTESIAN_POINT('Origin',(0.,0.,0.)) ;
#24380=CARTESIAN_POINT('Origin',(0.,1.6,0.)) ;
#24381=CARTESIAN_POINT('Origin',(0.325,-0.265,0.562916512459885)) ;
#24382=CARTESIAN_POINT('',(0.,-0.53,0.750555349946514)) ;
#24383=CARTESIAN_POINT('',(0.,0.,0.750555349946514)) ;
#24384=CARTESIAN_POINT('',(0.,-0.265,0.750555349946514)) ;
#24385=CARTESIAN_POINT('',(0.65,-0.53,0.375277674973257)) ;
#24386=CARTESIAN_POINT('',(0.325,-0.53,0.562916512459885)) ;
#24387=CARTESIAN_POINT('',(0.65,0.,0.375277674973257)) ;
#24388=CARTESIAN_POINT('',(0.65,-0.265,0.375277674973257)) ;
#24389=CARTESIAN_POINT('',(0.325,0.,0.562916512459885)) ;
#24390=CARTESIAN_POINT('Origin',(-0.325,-0.265,-0.562916512459885)) ;
#24391=CARTESIAN_POINT('',(0.,-0.53,-0.750555349946514)) ;
#24392=CARTESIAN_POINT('',(0.,0.,-0.750555349946514)) ;
#24393=CARTESIAN_POINT('',(0.,-0.265,-0.750555349946514)) ;
#24394=CARTESIAN_POINT('',(-0.65,-0.53,-0.375277674973257)) ;
#24395=CARTESIAN_POINT('',(-0.325,-0.53,-0.562916512459885)) ;
#24396=CARTESIAN_POINT('',(-0.65,0.,-0.375277674973257)) ;
#24397=CARTESIAN_POINT('',(-0.65,-0.265,-0.375277674973257)) ;
#24398=CARTESIAN_POINT('',(-0.325,0.,-0.562916512459885)) ;
#24399=CARTESIAN_POINT('Origin',(0.,-0.53,0.)) ;
#24400=CARTESIAN_POINT('',(-0.65,-0.53,0.375277674973257)) ;
#24401=CARTESIAN_POINT('',(-0.325,-0.53,0.562916512459885)) ;
#24402=CARTESIAN_POINT('',(-0.65,-0.53,0.)) ;
#24403=CARTESIAN_POINT('',(0.65,-0.53,-0.375277674973257)) ;
#24404=CARTESIAN_POINT('',(0.325,-0.53,-0.562916512459885)) ;
#24405=CARTESIAN_POINT('',(0.65,-0.53,0.)) ;
#24406=CARTESIAN_POINT('Origin',(-0.325,-0.265,0.562916512459885)) ;
#24407=CARTESIAN_POINT('',(-0.65,0.,0.375277674973257)) ;
#24408=CARTESIAN_POINT('',(-0.65,-0.265,0.375277674973257)) ;
#24409=CARTESIAN_POINT('',(-0.325,0.,0.562916512459885)) ;
#24410=CARTESIAN_POINT('Origin',(0.325,-0.265,-0.562916512459885)) ;
#24411=CARTESIAN_POINT('',(0.65,0.,-0.375277674973257)) ;
#24412=CARTESIAN_POINT('',(0.65,-0.265,-0.375277674973257)) ;
#24413=CARTESIAN_POINT('',(0.325,0.,-0.562916512459885)) ;
#24414=CARTESIAN_POINT('Origin',(-0.65,-0.265,0.)) ;
#24415=CARTESIAN_POINT('',(-0.65,0.,0.)) ;
#24416=CARTESIAN_POINT('Origin',(0.65,-0.265,0.)) ;
#24417=CARTESIAN_POINT('',(0.65,0.,0.)) ;
#24418=CARTESIAN_POINT('Origin',(0.,0.,0.)) ;
#24577=UNCERTAINTY_MEASURE_WITH_UNIT(LENGTH_MEASURE(0.001),#24629,
'DISTANCE_ACCURACY_VALUE',
'Maximum model space distance between geometric entities at asserted c
onnectivities') ;
#24580=UNCERTAINTY_MEASURE_WITH_UNIT(LENGTH_MEASURE(0.001),#24629,
'DISTANCE_ACCURACY_VALUE',
'Maximum model space distance between geometric entities at asserted c
onnectivities') ;
#24625=(
GEOMETRIC_REPRESENTATION_CONTEXT(3)
GLOBAL_UNCERTAINTY_ASSIGNED_CONTEXT((#24577))
GLOBAL_UNIT_ASSIGNED_CONTEXT((#24629,#24631,#24632))
REPRESENTATION_CONTEXT('','3D')
) ;
#24628=(
GEOMETRIC_REPRESENTATION_CONTEXT(3)
GLOBAL_UNCERTAINTY_ASSIGNED_CONTEXT((#24580))
GLOBAL_UNIT_ASSIGNED_CONTEXT((#24629,#24631,#24632))
REPRESENTATION_CONTEXT('','3D')
) ;
#24629=(
LENGTH_UNIT()
NAMED_UNIT(*)
SI_UNIT(.CENTI.,.METRE.)
) ;
#24631=(
NAMED_UNIT(*)
PLANE_ANGLE_UNIT()
SI_UNIT($,.RADIAN.)
) ;
#24632=(
NAMED_UNIT(*)
SI_UNIT($,.STERADIAN.)
SOLID_ANGLE_UNIT()
) ;
#24677=SHAPE_DEFINITION_REPRESENTATION(#24765,#24835) ;
#24765=PRODUCT_DEFINITION_SHAPE('',$,#24883) ;
#24835=SHAPE_REPRESENTATION('',(#15329),#24625) ;
#24838=PRODUCT_DEFINITION_CONTEXT('part definition',#24981,'design') ;
#24883=PRODUCT_DEFINITION('BRACKET_BOLT_M8x16',
'BRACKET_BOLT_M8x16',#24930,#24838) ;
#24930=PRODUCT_DEFINITION_FORMATION('',$,#25027) ;
#24981=APPLICATION_CONTEXT(
'Core Data for Automotive Mechanical Design Process') ;
#24982=PRODUCT_CONTEXT('part definition',#24981,'mechanical') ;
#25027=PRODUCT('BRACKET_BOLT_M8x16','BRACKET_BOLT_M8x16',$,(#24982)) ;
#25030=PRESENTATION_STYLE_ASSIGNMENT((#25040)) ;
#25040=SURFACE_STYLE_USAGE(.BOTH.,#25050) ;
#25050=SURFACE_SIDE_STYLE('',(#25060)) ;
#25060=SURFACE_STYLE_FILL_AREA(#25070) ;
#25070=FILL_AREA_STYLE('Steel - Satin',(#25080)) ;
#25080=FILL_AREA_STYLE_COLOUR('Steel - Satin',#25090) ;
#25090=COLOUR_RGB('Steel - Satin', 0.66274510, 0.83137255, 0.94901961) ;
ENDSEC;
END-ISO-10303-21;
